ISO-10303-21;
HEADER;
FILE_DESCRIPTION (('STEP AP214'),
    '1' );
FILE_NAME ('Tool Retaining Set Screws.step',
    '2026-10-08T01:23:29',
    ( '' ),
    ( '' ),
    'SwSTEP 2.0',
    'SolidWorks 2025',
    '' );
FILE_SCHEMA (( 'AUTOMOTIVE_DESIGN' ));
ENDSEC;

DATA;
#1=PLANE ( 'NONE',  #17713 ) ;
#295=DIRECTION ( 'NONE',  ( -0.5315839928299663786, 0.000000000000000000, 0.8470055835512245723 ) ) ;
#456=( NAMED_UNIT ( * ) SI_UNIT ( $, .STERADIAN. ) SOLID_ANGLE_UNIT ( ) );
#618=ORIENTED_EDGE ( 'NONE', *, *, #18542, .T. ) ;
#737=SURFACE_STYLE_FILL_AREA ( #32790 ) ;
#745=DIRECTION ( 'NONE',  ( -0.000000000000000000, -1.000000000000000000, -0.000000000000000000 ) ) ;
#881=AXIS2_PLACEMENT_3D ( 'NONE', #18199, #1900, #2427 ) ;
#920=ORIENTED_EDGE ( 'NONE', *, *, #23700, .F. ) ;
#1224=ORIENTED_EDGE ( 'NONE', *, *, #4058, .T. ) ;
#1241=EDGE_LOOP ( 'NONE', ( #25430, #19183, #25852, #22627 ) ) ;
#1256=ORIENTED_EDGE ( 'NONE', *, *, #9263, .T. ) ;
#1414=EDGE_CURVE ( 'NONE', #46358, #8157, #21568, .T. ) ;
#1508=CARTESIAN_POINT ( 'NONE',  ( 1.707904493811027491, 28.00000000000000355, -46.30033279450969985 ) ) ;
#1515=VERTEX_POINT ( 'NONE', #19036 ) ;
#1528=DIRECTION ( 'NONE',  ( 0.000000000000000000, 1.000000000000000000, 0.000000000000000000 ) ) ;
#1593=AXIS2_PLACEMENT_3D ( 'NONE', #30422, #5766, #33348 ) ;
#1623=PLANE ( 'NONE',  #24598 ) ;
#1630=VECTOR ( 'NONE', #5258, 1000.000000000000227 ) ;
#1642=CARTESIAN_POINT ( 'NONE',  ( 46.00000000000000711, 33.00000000000000000, -46.00000000000000000 ) ) ;
#1667=DIRECTION ( 'NONE',  ( -0.000000000000000000, -1.000000000000000000, -0.000000000000000000 ) ) ;
#1718=ORIENTED_EDGE ( 'NONE', *, *, #41687, .T. ) ;
#1741=DIRECTION ( 'NONE',  ( 0.000000000000000000, 0.000000000000000000, -1.000000000000000000 ) ) ;
#1776=DIRECTION ( 'NONE',  ( -0.4677363560876381943, 0.000000000000000000, -0.8838680338115290080 ) ) ;
#1836=VECTOR ( 'NONE', #25683, 1000.000000000000000 ) ;
#1900=DIRECTION ( 'NONE',  ( -1.000000000000000000, 0.000000000000000000, 0.000000000000000000 ) ) ;
#1905=ORIENTED_EDGE ( 'NONE', *, *, #46481, .T. ) ;
#2027=VERTEX_POINT ( 'NONE', #3973 ) ;
#2397=VECTOR ( 'NONE', #6564, 1000.000000000000000 ) ;
#2427=DIRECTION ( 'NONE',  ( 0.000000000000000000, 0.000000000000000000, 1.000000000000000000 ) ) ;
#2457=MECHANICAL_DESIGN_GEOMETRIC_PRESENTATION_REPRESENTATION('',(#36817),#33523);
#2498=LINE ( 'NONE', #6957, #12376 ) ;
#2786=DIRECTION ( 'NONE',  ( 0.000000000000000000, 0.000000000000000000, 1.000000000000000000 ) ) ;
#2900=DIRECTION ( 'NONE',  ( 0.000000000000000000, 0.000000000000000000, 1.000000000000000000 ) ) ;
#3232=DIRECTION ( 'NONE',  ( -0.4216675885939772384, 0.4327645661435913227, -0.7968131995768452658 ) ) ;
#3483=FACE_OUTER_BOUND ( 'NONE', #8475, .T. ) ;
#3539=DIRECTION ( 'NONE',  ( 0.8980129913408354536, 0.4399689391117108661, 0.000000000000000000 ) ) ;
#3703=CARTESIAN_POINT ( 'NONE',  ( 47.53769253747992707, 28.00000000000000355, -45.94327833438006081 ) ) ;
#3714=CARTESIAN_POINT ( 'NONE',  ( 0.000000000000000000, 0.000000000000000000, 0.000000000000000000 ) ) ;
#3862=CARTESIAN_POINT ( 'NONE',  ( 40.29886924377099433, 35.00000000000000000, -46.21030057994576623 ) ) ;
#3894=CIRCLE ( 'NONE', #19867, 4.999999999999997335 ) ;
#3929=LINE ( 'NONE', #19182, #43301 ) ;
#3973=CARTESIAN_POINT ( 'NONE',  ( 40.29886924377099433, 35.00000000000000000, -46.21030057994576623 ) ) ;
#3979=DIRECTION ( 'NONE',  ( 0.000000000000000000, 0.000000000000000000, 1.000000000000000000 ) ) ;
#4058=EDGE_CURVE ( 'NONE', #2027, #33969, #47760, .T. ) ;
#4237=CARTESIAN_POINT ( 'NONE',  ( 46.00000000000000711, -43.50000000000000000, -46.00000000000000000 ) ) ;
#4281=ORIENTED_EDGE ( 'NONE', *, *, #43355, .F. ) ;
#4353=CIRCLE ( 'NONE', #32853, 10.99999999999999645 ) ;
#4372=VECTOR ( 'NONE', #3232, 1000.000000000000227 ) ;
#4465=VECTOR ( 'NONE', #38777, 1000.000000000000227 ) ;
#4483=ADVANCED_FACE ( 'NONE', ( #5102 ), #32932, .F. ) ;
#4523=VECTOR ( 'NONE', #15969, 1000.000000000000227 ) ;
#4601=ORIENTED_EDGE ( 'NONE', *, *, #26721, .T. ) ;
#4736=ORIENTED_EDGE ( 'NONE', *, *, #46158, .F. ) ;
#4785=ADVANCED_FACE ( 'NONE', ( #23455 ), #41749, .F. ) ;
#4876=CIRCLE ( 'NONE', #24152, 4.000000000000003553 ) ;
#4883=FACE_BOUND ( 'NONE', #51499, .T. ) ;
#4938=LINE ( 'NONE', #13054, #25935 ) ;
#4952=FILL_AREA_STYLE_COLOUR ( '', #7451 ) ;
#5063=DIRECTION ( 'NONE',  ( 0.000000000000000000, 1.000000000000000000, 0.000000000000000000 ) ) ;
#5102=FACE_OUTER_BOUND ( 'NONE', #18635, .T. ) ;
#5247=LINE ( 'NONE', #25721, #43299 ) ;
#5258=DIRECTION ( 'NONE',  ( 0.5315839928299667116, 0.000000000000000000, -0.8470055835512242393 ) ) ;
#5313=CARTESIAN_POINT ( 'NONE',  ( 42.96730897722186171, 30.00000000000000355, -41.16782622478179832 ) ) ;
#5319=CARTESIAN_POINT ( 'NONE',  ( 46.00000000000000711, -42.50000000000000000, -41.00000000000000000 ) ) ;
#5399=PLANE ( 'NONE',  #35810 ) ;
#5628=DIRECTION ( 'NONE',  ( 0.4792266786073201557, 0.4327645661435911562, -0.7635814434633318992 ) ) ;
#5766=DIRECTION ( 'NONE',  ( -0.4285077258200425399, -0.8746197071393964073, 0.2267630851702541195 ) ) ;
#5809=CARTESIAN_POINT ( 'NONE',  ( 49.03269102277813829, 30.00000000000000355, -50.83217377521822300 ) ) ;
#5866=DIRECTION ( 'NONE',  ( -0.000000000000000000, -1.000000000000000000, -0.000000000000000000 ) ) ;
#5937=EDGE_CURVE ( 'NONE', #39637, #27204, #22632, .T. ) ;
#5940=DIRECTION ( 'NONE',  ( 0.000000000000000000, -1.000000000000000000, 0.000000000000000000 ) ) ;
#6070=CARTESIAN_POINT ( 'NONE',  ( 53.77560546639968919, 28.00000000000000355, -28.45764841024206504 ) ) ;
#6142=LINE ( 'NONE', #41089, #36495 ) ;
#6148=VERTEX_POINT ( 'NONE', #13641 ) ;
#6193=FACE_OUTER_BOUND ( 'NONE', #42111, .T. ) ;
#6365=ORIENTED_EDGE ( 'NONE', *, *, #45942, .F. ) ;
#6564=DIRECTION ( 'NONE',  ( -0.000000000000000000, 1.000000000000000000, -0.000000000000000000 ) ) ;
#6708=EDGE_LOOP ( 'NONE', ( #44032, #44875 ) ) ;
#6744=CARTESIAN_POINT ( 'NONE',  ( 51.70113075622899856, 35.00000000000000000, -45.78969942005421956 ) ) ;
#6792=CIRCLE ( 'NONE', #881, 2.000000000000001776 ) ;
#6843=( LENGTH_UNIT ( ) NAMED_UNIT ( * ) SI_UNIT ( .MILLI., .METRE. ) );
#6957=CARTESIAN_POINT ( 'NONE',  ( 11.16082883019764793, 28.00000000000000355, 7.004579506989120574 ) ) ;
#6994=DIRECTION ( 'NONE',  ( 0.000000000000000000, 0.000000000000000000, 1.000000000000000000 ) ) ;
#7082=EDGE_LOOP ( 'NONE', ( #27727, #23227, #43906, #33346, #11271, #33177 ) ) ;
#7381=FACE_OUTER_BOUND ( 'NONE', #33340, .T. ) ;
#7440=CARTESIAN_POINT ( 'NONE',  ( 44.41590053910517355, 28.88712326890129845, -48.99342751026321707 ) ) ;
#7451=COLOUR_RGB ( '', 0.08235294, 0.09019608, 0.10196078) ;
#7476=PRODUCT_DEFINITION_CONTEXT ( 'detailed design', #35726, 'design' ) ;
#7564=ORIENTED_EDGE ( 'NONE', *, *, #24403, .F. ) ;
#7599=AXIS2_PLACEMENT_3D ( 'NONE', #41849, #5866, #37901 ) ;
#7614=CARTESIAN_POINT ( 'NONE',  ( 46.00000000000000711, -42.50000000000000000, -46.00000000000000000 ) ) ;
#7843=ORIENTED_EDGE ( 'NONE', *, *, #37059, .F. ) ;
#7904=FACE_OUTER_BOUND ( 'NONE', #31705, .T. ) ;
#7936=DIRECTION ( 'NONE',  ( -0.4106364553079954738, -0.8746197071393962963, -0.2577170336929270333 ) ) ;
#7982=EDGE_CURVE ( 'NONE', #41636, #11274, #51473, .T. ) ;
#8004=DIRECTION ( 'NONE',  ( 0.000000000000000000, 1.000000000000000000, 0.000000000000000000 ) ) ;
#8107=CIRCLE ( 'NONE', #13188, 9.000000000000001776 ) ;
#8121=EDGE_CURVE ( 'NONE', #39858, #22860, #22519, .T. ) ;
#8157=VERTEX_POINT ( 'NONE', #23535 ) ;
#8438=DIRECTION ( 'NONE',  ( 1.000000000000000000, 0.000000000000000000, 0.000000000000000000 ) ) ;
#8470=ORIENTED_EDGE ( 'NONE', *, *, #46481, .F. ) ;
#8475=EDGE_LOOP ( 'NONE', ( #35977, #50474, #43778, #34501 ) ) ;
#8643=DIRECTION ( 'NONE',  ( 0.000000000000000000, 0.000000000000000000, 1.000000000000000000 ) ) ;
#8653=ORIENTED_EDGE ( 'NONE', *, *, #44578, .F. ) ;
#8680=TOROIDAL_SURFACE ( 'NONE', #43943, 9.000000000000000000, 2.000000000000000000 ) ;
#8866=APPLICATION_CONTEXT ( 'automotive_design' ) ;
#8936=DIRECTION ( 'NONE',  ( -0.000000000000000000, 1.000000000000000000, -0.000000000000000000 ) ) ;
#8991=EDGE_CURVE ( 'NONE', #28728, #41453, #22504, .T. ) ;
#8994=AXIS2_PLACEMENT_3D ( 'NONE', #51311, #31063, #15061 ) ;
#9263=EDGE_CURVE ( 'NONE', #12238, #46358, #20711, .T. ) ;
#9303=EDGE_CURVE ( 'NONE', #41107, #51365, #46390, .T. ) ;
#9412=ORIENTED_EDGE ( 'NONE', *, *, #14430, .T. ) ;
#9725=DIRECTION ( 'NONE',  ( -0.9993203489176063492, 0.000000000000000000, -0.03686245026030391531 ) ) ;
#9776=FACE_OUTER_BOUND ( 'NONE', #12631, .T. ) ;
#9814=CARTESIAN_POINT ( 'NONE',  ( 49.03269102277813829, 30.00000000000000355, -50.83217377521822300 ) ) ;
#9841=EDGE_LOOP ( 'NONE', ( #618, #48341, #49336, #50336 ) ) ;
#10025=( NAMED_UNIT ( * ) SI_UNIT ( $, .STERADIAN. ) SOLID_ANGLE_UNIT ( ) );
#10229=LINE ( 'NONE', #26248, #2397 ) ;
#10443=EDGE_LOOP ( 'NONE', ( #1224, #8653, #6365, #47293 ) ) ;
#10536=AXIS2_PLACEMENT_3D ( 'NONE', #13352, #38732, #14586 ) ;
#10588=VECTOR ( 'NONE', #43040, 1000.000000000000000 ) ;
#10594=VECTOR ( 'NONE', #295, 1000.000000000000114 ) ;
#10642=DIRECTION ( 'NONE',  ( -0.000000000000000000, 1.000000000000000000, -0.000000000000000000 ) ) ;
#10725=ORIENTED_EDGE ( 'NONE', *, *, #18542, .F. ) ;
#10731=ADVANCED_FACE ( 'NONE', ( #27354 ), #39683, .F. ) ;
#10765=ADVANCED_FACE ( 'NONE', ( #48904 ), #49162, .F. ) ;
#10797=CARTESIAN_POINT ( 'NONE',  ( 46.00000000000000711, -43.50000000000000000, -41.99999999999999289 ) ) ;
#10807=VECTOR ( 'NONE', #17036, 1000.000000000000227 ) ;
#10946=DIRECTION ( 'NONE',  ( 0.000000000000000000, -1.000000000000000000, 0.000000000000000000 ) ) ;
#11139=CLOSED_SHELL ( 'NONE', ( #20890, #28797, #37961, #17608, #41968, #18010, #12995, #21531, #12824, #43779, #19886, #20350, #21982, #10731, #10765, #4483, #34353, #26007, #4785, #31352, #26245, #25529, #15629, #38744 ) ) ;
#11148=DIRECTION ( 'NONE',  ( -0.000000000000000000, -1.000000000000000000, -0.000000000000000000 ) ) ;
#11271=ORIENTED_EDGE ( 'NONE', *, *, #18657, .T. ) ;
#11274=VERTEX_POINT ( 'NONE', #41800 ) ;
#11417=CARTESIAN_POINT ( 'NONE',  ( 51.70113075622899856, 30.00000000000000355, -45.78969942005421956 ) ) ;
#11639=SHAPE_REPRESENTATION ( 'Tool Retaining Set Screws', ( #31742 ), #22569 ) ;
#11721=DIRECTION ( 'NONE',  ( 0.000000000000000000, -0.000000000000000000, 1.000000000000000000 ) ) ;
#11755=ORIENTED_EDGE ( 'NONE', *, *, #24086, .T. ) ;
#11774=CARTESIAN_POINT ( 'NONE',  ( 51.70113075622899856, 30.00000000000000355, -45.78969942005421956 ) ) ;
#12095=EDGE_CURVE ( 'NONE', #35357, #1515, #33504, .T. ) ;
#12106=DIRECTION ( 'NONE',  ( 0.9993203489176063492, 0.000000000000000000, 0.03686245026030503941 ) ) ;
#12238=VERTEX_POINT ( 'NONE', #18788 ) ;
#12247=DIRECTION ( 'NONE',  ( 0.4677363560876406923, 0.000000000000000000, 0.8838680338115276758 ) ) ;
#12250=VECTOR ( 'NONE', #32538, 1000.000000000000227 ) ;
#12275=AXIS2_PLACEMENT_3D ( 'NONE', #34298, #10642, #14332 ) ;
#12287=LINE ( 'NONE', #28318, #18378 ) ;
#12376=VECTOR ( 'NONE', #50594, 1000.000000000000114 ) ;
#12631=EDGE_LOOP ( 'NONE', ( #24281, #48634, #7564, #33691 ) ) ;
#12642=EDGE_CURVE ( 'NONE', #22860, #48670, #21225, .T. ) ;
#12696=EDGE_CURVE ( 'NONE', #34751, #33745, #41182, .T. ) ;
#12824=ADVANCED_FACE ( 'NONE', ( #15160 ), #38016, .T. ) ;
#12995=ADVANCED_FACE ( 'NONE', ( #32469, #43252 ), #23307, .F. ) ;
#13054=CARTESIAN_POINT ( 'NONE',  ( 46.00000000000000711, -57.64213562373095101, -51.00000000000000000 ) ) ;
#13153=CARTESIAN_POINT ( 'NONE',  ( 43.33156026654913262, 30.00000000000000355, -51.04247435516399634 ) ) ;
#13188=AXIS2_PLACEMENT_3D ( 'NONE', #51642, #8004, #31662 ) ;
#13245=AXIS2_PLACEMENT_3D ( 'NONE', #13153, #37839, #49436 ) ;
#13277=DIRECTION ( 'NONE',  ( 0.000000000000000000, 1.000000000000000000, 0.000000000000000000 ) ) ;
#13352=CARTESIAN_POINT ( 'NONE',  ( 46.00000000000000711, -43.50000000000000000, -46.00000000000000000 ) ) ;
#13424=AXIS2_PLACEMENT_3D ( 'NONE', #43526, #39318, #35897 ) ;
#13448=PLANE ( 'NONE',  #49563 ) ;
#13498=EDGE_CURVE ( 'NONE', #12238, #27379, #6792, .T. ) ;
#13584=EDGE_CURVE ( 'NONE', #41636, #12238, #38653, .T. ) ;
#13641=CARTESIAN_POINT ( 'NONE',  ( 40.29886924377099433, 30.00000000000000355, -46.21030057994576623 ) ) ;
#13844=PRODUCT ( 'Tool Retaining Set Screws', 'Tool Retaining Set Screws', '', ( #24948 ) ) ;
#13860=VECTOR ( 'NONE', #1776, 1000.000000000000000 ) ;
#13961=DIRECTION ( 'NONE',  ( -0.4677363560876381943, 0.000000000000000000, -0.8838680338115290080 ) ) ;
#14009=ORIENTED_EDGE ( 'NONE', *, *, #48592, .T. ) ;
#14054=EDGE_CURVE ( 'NONE', #51208, #44162, #26257, .T. ) ;
#14128=AXIS2_PLACEMENT_3D ( 'NONE', #45561, #1667, #33968 ) ;
#14332=DIRECTION ( 'NONE',  ( 0.000000000000000000, 0.000000000000000000, 1.000000000000000000 ) ) ;
#14378=EDGE_LOOP ( 'NONE', ( #37693, #48654, #15338, #45853 ) ) ;
#14404=ORIENTED_EDGE ( 'NONE', *, *, #14054, .T. ) ;
#14430=EDGE_CURVE ( 'NONE', #39637, #28728, #33189, .T. ) ;
#14570=DIRECTION ( 'NONE',  ( 0.000000000000000000, -1.000000000000000000, -0.000000000000000000 ) ) ;
#14586=DIRECTION ( 'NONE',  ( 0.000000000000000000, 0.000000000000000000, -1.000000000000000000 ) ) ;
#14605=DIRECTION ( 'NONE',  ( 8.659560562354930393E-17, 0.7071067811865479058, -0.7071067811865472397 ) ) ;
#14854=UNCERTAINTY_MEASURE_WITH_UNIT (LENGTH_MEASURE( 1.000000000000000082E-05 ), #6843, 'distance_accuracy_value', 'NONE');
#14925=CARTESIAN_POINT ( 'NONE',  ( 46.00000000000000711, -42.50000000000000000, -51.00000000000000000 ) ) ;
#15061=DIRECTION ( 'NONE',  ( 0.9993203489176063492, 0.000000000000000000, 0.03686245026030503941 ) ) ;
#15121=CYLINDRICAL_SURFACE ( 'NONE', #37127, 10.99999999999999645 ) ;
#15160=FACE_OUTER_BOUND ( 'NONE', #27739, .T. ) ;
#15268=LINE ( 'NONE', #27609, #26856 ) ;
#15314=LINE ( 'NONE', #7440, #4372 ) ;
#15338=ORIENTED_EDGE ( 'NONE', *, *, #50136, .T. ) ;
#15423=LINE ( 'NONE', #31428, #50297 ) ;
#15435=ORIENTED_EDGE ( 'NONE', *, *, #50700, .T. ) ;
#15500=DIRECTION ( 'NONE',  ( -0.000000000000000000, 1.000000000000000000, -0.000000000000000000 ) ) ;
#15540=DIRECTION ( 'NONE',  ( 0.4677363560876406923, 0.000000000000000000, 0.8838680338115275648 ) ) ;
#15556=LINE ( 'NONE', #23189, #40754 ) ;
#15629=ADVANCED_FACE ( 'NONE', ( #23809 ), #16193, .T. ) ;
#15774=AXIS2_PLACEMENT_3D ( 'NONE', #47865, #36025, #15540 ) ;
#15836=CARTESIAN_POINT ( 'NONE',  ( 43.33156026654913262, 30.00000000000000355, -51.04247435516399634 ) ) ;
#15969=DIRECTION ( 'NONE',  ( 0.4216675885939766832, 0.4327645661435912672, 0.7968131995768455988 ) ) ;
#16045=TOROIDAL_SURFACE ( 'NONE', #45424, 9.000000000000000000, 2.000000000000000000 ) ;
#16078=DIRECTION ( 'NONE',  ( -0.9993203489176063492, 0.000000000000000000, -0.03686245026030392224 ) ) ;
#16081=LINE ( 'NONE', #20015, #40871 ) ;
#16193=PLANE ( 'NONE',  #45703 ) ;
#16228=CARTESIAN_POINT ( 'NONE',  ( 43.33156026654913262, 35.00000000000000000, -51.04247435516399634 ) ) ;
#16360=VERTEX_POINT ( 'NONE', #3703 ) ;
#16482=CARTESIAN_POINT ( 'NONE',  ( 47.58409946089483356, 28.88712326890129489, -43.00657248973679714 ) ) ;
#16827=ORIENTED_EDGE ( 'NONE', *, *, #1414, .T. ) ;
#17036=DIRECTION ( 'NONE',  ( -0.9993203489176063492, 0.000000000000000000, -0.03686245026030391531 ) ) ;
#17069=VECTOR ( 'NONE', #46535, 1000.000000000000000 ) ;
#17181=EDGE_CURVE ( 'NONE', #46692, #25869, #15556, .T. ) ;
#17277=DIRECTION ( 'NONE',  ( -0.000000000000000000, 1.000000000000000000, -0.000000000000000000 ) ) ;
#17284=ORIENTED_EDGE ( 'NONE', *, *, #26721, .F. ) ;
#17397=DIRECTION ( 'NONE',  ( 0.4677363560876406923, 0.000000000000000000, 0.8838680338115276758 ) ) ;
#17564=AXIS2_PLACEMENT_3D ( 'NONE', #17764, #5940, #30349 ) ;
#17608=ADVANCED_FACE ( 'NONE', ( #47821 ), #23881, .T. ) ;
#17713=AXIS2_PLACEMENT_3D ( 'NONE', #18937, #39159, #19971 ) ;
#17764=CARTESIAN_POINT ( 'NONE',  ( 46.00000000000000711, 20.00000000000000000, -46.00000000000000000 ) ) ;
#18010=ADVANCED_FACE ( 'NONE', ( #4883, #20910 ), #5399, .T. ) ;
#18199=CARTESIAN_POINT ( 'NONE',  ( 46.00000000000000711, 33.00000000000000000, -37.00000000000000000 ) ) ;
#18231=CONICAL_SURFACE ( 'NONE', #43395, 4.000000000000003553, 0.7853981633974479459 ) ;
#18283=CYLINDRICAL_SURFACE ( 'NONE', #12275, 4.999999999999997335 ) ;
#18369=VECTOR ( 'NONE', #47802, 1000.000000000000227 ) ;
#18378=VECTOR ( 'NONE', #19655, 1000.000000000000114 ) ;
#18391=CARTESIAN_POINT ( 'NONE',  ( 46.00000000000000711, 20.00000000000000000, -41.00000000000000000 ) ) ;
#18408=ORIENTED_EDGE ( 'NONE', *, *, #8991, .F. ) ;
#18468=AXIS2_PLACEMENT_3D ( 'NONE', #37304, #8936, #29161 ) ;
#18542=EDGE_CURVE ( 'NONE', #33969, #30895, #16081, .T. ) ;
#18585=CARTESIAN_POINT ( 'NONE',  ( 44.46230746252008004, 28.00000000000000355, -46.05672166561993208 ) ) ;
#18635=EDGE_LOOP ( 'NONE', ( #38272, #38514, #38884, #45810 ) ) ;
#18657=EDGE_CURVE ( 'NONE', #51239, #34751, #21317, .T. ) ;
#18788=CARTESIAN_POINT ( 'NONE',  ( 46.00000000000000711, 33.00000000000000000, -35.00000000000000000 ) ) ;
#18812=DIRECTION ( 'NONE',  ( 0.000000000000000000, 0.000000000000000000, -1.000000000000000000 ) ) ;
#18826=CARTESIAN_POINT ( 'NONE',  ( 46.00000000000000711, 20.00000000000000000, -46.00000000000000000 ) ) ;
#18937=CARTESIAN_POINT ( 'NONE',  ( 49.03269102277813829, 30.00000000000000355, -50.83217377521822300 ) ) ;
#18950=DIRECTION ( 'NONE',  ( -0.000000000000000000, 1.000000000000000000, -0.000000000000000000 ) ) ;
#19036=CARTESIAN_POINT ( 'NONE',  ( 46.00000000000000711, 20.00000000000000000, -51.00000000000000000 ) ) ;
#19182=CARTESIAN_POINT ( 'NONE',  ( 48.66843973345087448, 30.00000000000000355, -40.95752564483601788 ) ) ;
#19183=ORIENTED_EDGE ( 'NONE', *, *, #39738, .F. ) ;
#19286=AXIS2_PLACEMENT_3D ( 'NONE', #46965, #10946, #26965 ) ;
#19326=FACE_OUTER_BOUND ( 'NONE', #50106, .T. ) ;
#19514=EDGE_LOOP ( 'NONE', ( #4601, #35877, #46739, #43915 ) ) ;
#19618=CARTESIAN_POINT ( 'NONE',  ( 49.03269102277813829, 30.00000000000000355, -50.83217377521822300 ) ) ;
#19655=DIRECTION ( 'NONE',  ( -0.4792266786073193785, 0.4327645661435916002, 0.7635814434633321213 ) ) ;
#19672=LINE ( 'NONE', #27564, #27273 ) ;
#19820=ORIENTED_EDGE ( 'NONE', *, *, #12095, .T. ) ;
#19867=AXIS2_PLACEMENT_3D ( 'NONE', #33283, #25653, #1741 ) ;
#19886=ADVANCED_FACE ( 'NONE', ( #30246 ), #1623, .F. ) ;
#19898=ORIENTED_EDGE ( 'NONE', *, *, #8121, .F. ) ;
#19971=DIRECTION ( 'NONE',  ( 0.000000000000000000, 0.4845575045900850641, -0.8747594096352605542 ) ) ;
#19987=ORIENTED_EDGE ( 'NONE', *, *, #50700, .F. ) ;
#20015=CARTESIAN_POINT ( 'NONE',  ( 42.96730897722186171, 35.00000000000000000, -41.16782622478179832 ) ) ;
#20054=EDGE_LOOP ( 'NONE', ( #45484, #25922 ) ) ;
#20064=LINE ( 'NONE', #36091, #32433 ) ;
#20070=ORIENTED_EDGE ( 'NONE', *, *, #14430, .F. ) ;
#20187=ORIENTED_EDGE ( 'NONE', *, *, #47820, .F. ) ;
#20350=ADVANCED_FACE ( 'NONE', ( #50431 ), #29139, .F. ) ;
#20416=DIRECTION ( 'NONE',  ( -0.5315839928299663786, 0.000000000000000000, 0.8470055835512245723 ) ) ;
#20491=EDGE_CURVE ( 'NONE', #41453, #27204, #3894, .T. ) ;
#20539=EDGE_CURVE ( 'NONE', #37802, #41107, #20064, .T. ) ;
#20711=LINE ( 'NONE', #36747, #33227 ) ;
#20870=DIRECTION ( 'NONE',  ( 0.03686245026030392918, 0.000000000000000000, -0.9993203489176064602 ) ) ;
#20878=DIRECTION ( 'NONE',  ( 0.000000000000000000, 1.000000000000000000, 0.000000000000000000 ) ) ;
#20890=ADVANCED_FACE ( 'NONE', ( #7904 ), #18231, .T. ) ;
#20910=FACE_OUTER_BOUND ( 'NONE', #46021, .T. ) ;
#20955=LINE ( 'NONE', #16228, #40367 ) ;
#21179=CARTESIAN_POINT ( 'NONE',  ( 46.00000000000000711, 33.00000000000000000, -56.99999999999999289 ) ) ;
#21225=LINE ( 'NONE', #45159, #10807 ) ;
#21265=DIRECTION ( 'NONE',  ( 0.9008942672012963948, 0.4327645661435914337, 0.03323175611351393555 ) ) ;
#21317=LINE ( 'NONE', #6070, #22479 ) ;
#21362=AXIS2_PLACEMENT_3D ( 'NONE', #43946, #7936, #23969 ) ;
#21531=ADVANCED_FACE ( 'NONE', ( #6193 ), #18283, .T. ) ;
#21544=CARTESIAN_POINT ( 'NONE',  ( 48.66843973345087448, 35.00000000000000000, -40.95752564483601788 ) ) ;
#21568=CIRCLE ( 'NONE', #45059, 10.99999999999999645 ) ;
#21668=VECTOR ( 'NONE', #12247, 1000.000000000000000 ) ;
#21764=CARTESIAN_POINT ( 'NONE',  ( 56.13126667599141939, 28.00000000000000355, -29.70424671247935677 ) ) ;
#21875=ORIENTED_EDGE ( 'NONE', *, *, #30251, .T. ) ;
#21982=ADVANCED_FACE ( 'NONE', ( #43147 ), #23452, .F. ) ;
#22294=CARTESIAN_POINT ( 'NONE',  ( 46.00000000000000711, 20.00000000000000000, -46.00000000000000000 ) ) ;
#22336=ORIENTED_EDGE ( 'NONE', *, *, #13498, .T. ) ;
#22416=ORIENTED_EDGE ( 'NONE', *, *, #23134, .F. ) ;
#22479=VECTOR ( 'NONE', #17397, 1000.000000000000000 ) ;
#22504=LINE ( 'NONE', #50102, #49757 ) ;
#22519=LINE ( 'NONE', #6744, #4465 ) ;
#22569=( GEOMETRIC_REPRESENTATION_CONTEXT ( 3 ) GLOBAL_UNCERTAINTY_ASSIGNED_CONTEXT ( ( #14854 ) ) GLOBAL_UNIT_ASSIGNED_CONTEXT ( ( #6843, #42584, #10025 ) ) REPRESENTATION_CONTEXT ( 'NONE', 'WORKASPACE' ) );
#22627=ORIENTED_EDGE ( 'NONE', *, *, #23490, .T. ) ;
#22632=LINE ( 'NONE', #10797, #50149 ) ;
#22721=UNCERTAINTY_MEASURE_WITH_UNIT (LENGTH_MEASURE( 1.000000000000000082E-05 ), #29615, 'distance_accuracy_value', 'NONE');
#22766=CARTESIAN_POINT ( 'NONE',  ( 46.00000000000000711, 35.00000000000000000, -46.00000000000000000 ) ) ;
#22771=FACE_OUTER_BOUND ( 'NONE', #34566, .T. ) ;
#22860=VERTEX_POINT ( 'NONE', #39552 ) ;
#22880=DIRECTION ( 'NONE',  ( 0.000000000000000000, 0.7071067811865479058, 0.7071067811865472397 ) ) ;
#23134=EDGE_CURVE ( 'NONE', #28728, #39637, #4876, .T. ) ;
#23189=CARTESIAN_POINT ( 'NONE',  ( 1.806149300554621862, 28.00000000000000355, -48.96369439584437799 ) ) ;
#23227=ORIENTED_EDGE ( 'NONE', *, *, #47820, .T. ) ;
#23307=PLANE ( 'NONE',  #13424 ) ;
#23452=PLANE ( 'NONE',  #8994 ) ;
#23455=FACE_OUTER_BOUND ( 'NONE', #43589, .T. ) ;
#23490=EDGE_CURVE ( 'NONE', #51365, #39858, #10229, .T. ) ;
#23524=ORIENTED_EDGE ( 'NONE', *, *, #12642, .F. ) ;
#23535=CARTESIAN_POINT ( 'NONE',  ( 46.00000000000000711, 20.00000000000000000, -56.99999999999999289 ) ) ;
#23700=EDGE_CURVE ( 'NONE', #34751, #37802, #12287, .T. ) ;
#23809=FACE_OUTER_BOUND ( 'NONE', #7082, .T. ) ;
#23881=CYLINDRICAL_SURFACE ( 'NONE', #50914, 10.99999999999999645 ) ;
#23969=DIRECTION ( 'NONE',  ( 0.9051968626821054187, -0.4249925173346862373, 0.000000000000000000 ) ) ;
#24086=EDGE_CURVE ( 'NONE', #41453, #1515, #4938, .T. ) ;
#24152=AXIS2_PLACEMENT_3D ( 'NONE', #26118, #14570, #42147 ) ;
#24206=AXIS2_PLACEMENT_3D ( 'NONE', #9814, #20870, #45315 ) ;
#24281=ORIENTED_EDGE ( 'NONE', *, *, #13584, .F. ) ;
#24329=DIRECTION ( 'NONE',  ( 0.000000000000000000, 1.000000000000000000, 0.000000000000000000 ) ) ;
#24403=EDGE_CURVE ( 'NONE', #27379, #11274, #35689, .T. ) ;
#24421=DIRECTION ( 'NONE',  ( 0.000000000000000000, 0.000000000000000000, -1.000000000000000000 ) ) ;
#24598=AXIS2_PLACEMENT_3D ( 'NONE', #50488, #42317, #13961 ) ;
#24600=AXIS2_PLACEMENT_3D ( 'NONE', #26955, #42990, #18812 ) ;
#24633=EDGE_CURVE ( 'NONE', #44162, #48670, #37431, .T. ) ;
#24854=ORIENTED_EDGE ( 'NONE', *, *, #24086, .F. ) ;
#24860=CARTESIAN_POINT ( 'NONE',  ( 42.61556600127744332, 28.88712326890129845, -46.12484337987545757 ) ) ;
#24919=CARTESIAN_POINT ( 'NONE',  ( 48.66843973345087448, 30.00000000000000355, -40.95752564483601788 ) ) ;
#24948=PRODUCT_CONTEXT ( 'NONE', #8866, 'mechanical' ) ;
#25094=ORIENTED_EDGE ( 'NONE', *, *, #18657, .F. ) ;
#25174=PRESENTATION_STYLE_ASSIGNMENT (( #25427 ) ) ;
#25427=SURFACE_STYLE_USAGE ( .BOTH. , #40389 ) ;
#25430=ORIENTED_EDGE ( 'NONE', *, *, #8121, .T. ) ;
#25509=LINE ( 'NONE', #49454, #47999 ) ;
#25529=ADVANCED_FACE ( 'NONE', ( #19326 ), #47434, .F. ) ;
#25653=DIRECTION ( 'NONE',  ( 0.000000000000000000, 1.000000000000000000, 0.000000000000000000 ) ) ;
#25683=DIRECTION ( 'NONE',  ( -0.000000000000000000, 1.000000000000000000, -0.000000000000000000 ) ) ;
#25721=CARTESIAN_POINT ( 'NONE',  ( 49.38443399872257800, 28.88712326890130555, -45.87515662012453532 ) ) ;
#25852=ORIENTED_EDGE ( 'NONE', *, *, #36588, .F. ) ;
#25869=VERTEX_POINT ( 'NONE', #43439 ) ;
#25922=ORIENTED_EDGE ( 'NONE', *, *, #30251, .F. ) ;
#25935=VECTOR ( 'NONE', #17277, 1000.000000000000000 ) ;
#26007=ADVANCED_FACE ( 'NONE', ( #36570 ), #13448, .F. ) ;
#26118=CARTESIAN_POINT ( 'NONE',  ( 46.00000000000000711, -43.50000000000000000, -46.00000000000000000 ) ) ;
#26245=ADVANCED_FACE ( 'NONE', ( #7381 ), #1, .F. ) ;
#26248=CARTESIAN_POINT ( 'NONE',  ( 51.70113075622899856, 30.00000000000000355, -45.78969942005421956 ) ) ;
#26257=LINE ( 'NONE', #5809, #31490 ) ;
#26286=CARTESIAN_POINT ( 'NONE',  ( 40.29886924377099433, 30.00000000000000355, -46.21030057994576623 ) ) ;
#26678=DIRECTION ( 'NONE',  ( -0.9008942672012966169, 0.4327645661435913227, -0.03323175611351236042 ) ) ;
#26721=EDGE_CURVE ( 'NONE', #48670, #2027, #20955, .T. ) ;
#26749=CARTESIAN_POINT ( 'NONE',  ( 46.00000000000000711, 35.00000000000000000, -56.99999999999999289 ) ) ;
#26837=VECTOR ( 'NONE', #45408, 1000.000000000000227 ) ;
#26856=VECTOR ( 'NONE', #18950, 1000.000000000000000 ) ;
#26917=ORIENTED_EDGE ( 'NONE', *, *, #49994, .T. ) ;
#26955=CARTESIAN_POINT ( 'NONE',  ( 46.00000000000000711, 33.00000000000000000, -55.00000000000000000 ) ) ;
#26965=DIRECTION ( 'NONE',  ( 0.000000000000000000, 0.000000000000000000, -1.000000000000000000 ) ) ;
#27062=DIRECTION ( 'NONE',  ( 0.000000000000000000, 1.000000000000000000, 0.000000000000000000 ) ) ;
#27173=DIRECTION ( 'NONE',  ( 0.000000000000000000, 0.000000000000000000, -1.000000000000000000 ) ) ;
#27199=ORIENTED_EDGE ( 'NONE', *, *, #35864, .F. ) ;
#27204=VERTEX_POINT ( 'NONE', #5319 ) ;
#27212=ORIENTED_EDGE ( 'NONE', *, *, #37874, .F. ) ;
#27273=VECTOR ( 'NONE', #32016, 1000.000000000000000 ) ;
#27354=FACE_OUTER_BOUND ( 'NONE', #10443, .T. ) ;
#27379=VERTEX_POINT ( 'NONE', #30503 ) ;
#27436=ORIENTED_EDGE ( 'NONE', *, *, #9303, .T. ) ;
#27454=DIRECTION ( 'NONE',  ( 0.4285077258200430950, -0.8746197071393964073, -0.2267630851702529260 ) ) ;
#27491=DIRECTION ( 'NONE',  ( 0.000000000000000000, 0.000000000000000000, 1.000000000000000000 ) ) ;
#27564=CARTESIAN_POINT ( 'NONE',  ( 40.29886924377099433, 30.00000000000000355, -46.21030057994576623 ) ) ;
#27609=CARTESIAN_POINT ( 'NONE',  ( 46.00000000000000711, -57.64213562373095101, -41.00000000000000000 ) ) ;
#27727=ORIENTED_EDGE ( 'NONE', *, *, #35864, .T. ) ;
#27739=EDGE_LOOP ( 'NONE', ( #9412, #42182 ) ) ;
#27912=PLANE ( 'NONE',  #21362 ) ;
#28080=CARTESIAN_POINT ( 'NONE',  ( 46.00000000000000711, 20.00000000000000000, -46.00000000000000000 ) ) ;
#28318=CARTESIAN_POINT ( 'NONE',  ( 44.19966546217225556, 28.88712326890130555, -43.13141586961224050 ) ) ;
#28420=DIRECTION ( 'NONE',  ( 0.000000000000000000, 0.000000000000000000, -1.000000000000000000 ) ) ;
#28597=EDGE_LOOP ( 'NONE', ( #44231, #11755, #21875, #27212 ) ) ;
#28630=CYLINDRICAL_SURFACE ( 'NONE', #18468, 4.999999999999997335 ) ;
#28654=ORIENTED_EDGE ( 'NONE', *, *, #12696, .F. ) ;
#28728=VERTEX_POINT ( 'NONE', #49985 ) ;
#28797=ADVANCED_FACE ( 'NONE', ( #9776 ), #8680, .T. ) ;
#28828=ORIENTED_EDGE ( 'NONE', *, *, #49111, .T. ) ;
#28829=( NAMED_UNIT ( * ) PLANE_ANGLE_UNIT ( ) SI_UNIT ( $, .RADIAN. ) );
#29139=PLANE ( 'NONE',  #30741 ) ;
#29159=CARTESIAN_POINT ( 'NONE',  ( 42.96730897722186171, 35.00000000000000000, -41.16782622478179832 ) ) ;
#29161=DIRECTION ( 'NONE',  ( 0.000000000000000000, 0.000000000000000000, 1.000000000000000000 ) ) ;
#29296=PLANE ( 'NONE',  #41729 ) ;
#29310=ORIENTED_EDGE ( 'NONE', *, *, #5937, .F. ) ;
#29615=( LENGTH_UNIT ( ) NAMED_UNIT ( * ) SI_UNIT ( .MILLI., .METRE. ) );
#29616=CARTESIAN_POINT ( 'NONE',  ( 49.03269102277813829, 30.00000000000000355, -50.83217377521822300 ) ) ;
#29679=EDGE_LOOP ( 'NONE', ( #36778, #8470, #28654, #31689 ) ) ;
#30056=ORIENTED_EDGE ( 'NONE', *, *, #50136, .F. ) ;
#30246=FACE_OUTER_BOUND ( 'NONE', #1241, .T. ) ;
#30251=EDGE_CURVE ( 'NONE', #1515, #35357, #43227, .T. ) ;
#30255=CARTESIAN_POINT ( 'NONE',  ( 48.66843973345087448, 30.00000000000000355, -40.95752564483601788 ) ) ;
#30267=EDGE_LOOP ( 'NONE', ( #49223, #32215, #22336, #19987 ) ) ;
#30349=DIRECTION ( 'NONE',  ( 0.000000000000000000, 0.000000000000000000, -1.000000000000000000 ) ) ;
#30422=CARTESIAN_POINT ( 'NONE',  ( 40.29886924377099433, 30.00000000000000355, -46.21030057994576623 ) ) ;
#30503=CARTESIAN_POINT ( 'NONE',  ( 46.00000000000000711, 35.00000000000000000, -37.00000000000000000 ) ) ;
#30612=AXIS2_PLACEMENT_3D ( 'NONE', #22294, #38322, #28420 ) ;
#30626=PRODUCT_DEFINITION_SHAPE ( 'NONE', 'NONE',  #36651 ) ;
#30741=AXIS2_PLACEMENT_3D ( 'NONE', #46476, #46738, #35403 ) ;
#30895=VERTEX_POINT ( 'NONE', #31923 ) ;
#30922=DIRECTION ( 'NONE',  ( 0.000000000000000000, 1.000000000000000000, 0.000000000000000000 ) ) ;
#31063=DIRECTION ( 'NONE',  ( -0.03686245026030504635, 0.000000000000000000, 0.9993203489176064602 ) ) ;
#31249=DIRECTION ( 'NONE',  ( 0.000000000000000000, 0.000000000000000000, -1.000000000000000000 ) ) ;
#31352=ADVANCED_FACE ( 'NONE', ( #3483 ), #27912, .F. ) ;
#31428=CARTESIAN_POINT ( 'NONE',  ( 13.41824523304568828, 28.00000000000000355, 8.421342806086375532 ) ) ;
#31490=VECTOR ( 'NONE', #9725, 1000.000000000000227 ) ;
#31526=FACE_OUTER_BOUND ( 'NONE', #30267, .T. ) ;
#31662=DIRECTION ( 'NONE',  ( 0.000000000000000000, 0.000000000000000000, 1.000000000000000000 ) ) ;
#31689=ORIENTED_EDGE ( 'NONE', *, *, #23700, .T. ) ;
#31705=EDGE_LOOP ( 'NONE', ( #22416, #51098, #4736, #29310 ) ) ;
#31742=AXIS2_PLACEMENT_3D ( 'NONE', #3714, #31843, #8438 ) ;
#31783=DIRECTION ( 'NONE',  ( -0.000000000000000000, -1.000000000000000000, -0.000000000000000000 ) ) ;
#31843=DIRECTION ( 'NONE',  ( 0.000000000000000000, 0.000000000000000000, 1.000000000000000000 ) ) ;
#31869=CARTESIAN_POINT ( 'NONE',  ( 46.71972386536815236, 28.00000000000000355, -44.63995836652267712 ) ) ;
#31923=CARTESIAN_POINT ( 'NONE',  ( 48.66843973345087448, 35.00000000000000000, -40.95752564483601788 ) ) ;
#32016=DIRECTION ( 'NONE',  ( -0.000000000000000000, 1.000000000000000000, -0.000000000000000000 ) ) ;
#32215=ORIENTED_EDGE ( 'NONE', *, *, #51902, .F. ) ;
#32433=VECTOR ( 'NONE', #48457, 1000.000000000000227 ) ;
#32469=FACE_BOUND ( 'NONE', #20054, .T. ) ;
#32538=DIRECTION ( 'NONE',  ( 0.5315839928299667116, 0.000000000000000000, -0.8470055835512242393 ) ) ;
#32789=EDGE_LOOP ( 'NONE', ( #41810, #34855, #34188, #14009 ) ) ;
#32790=FILL_AREA_STYLE ('',( #4952 ) ) ;
#32853=AXIS2_PLACEMENT_3D ( 'NONE', #18826, #30922, #27491 ) ;
#32932=PLANE ( 'NONE',  #24206 ) ;
#32988=EDGE_CURVE ( 'NONE', #44162, #6148, #51561, .T. ) ;
#32992=LINE ( 'NONE', #24860, #47244 ) ;
#33177=ORIENTED_EDGE ( 'NONE', *, *, #12696, .T. ) ;
#33189=CIRCLE ( 'NONE', #10536, 4.000000000000003553 ) ;
#33227=VECTOR ( 'NONE', #745, 1000.000000000000000 ) ;
#33283=CARTESIAN_POINT ( 'NONE',  ( 46.00000000000000711, -42.50000000000000000, -46.00000000000000000 ) ) ;
#33340=EDGE_LOOP ( 'NONE', ( #14404, #4281, #34648, #28828 ) ) ;
#33346=ORIENTED_EDGE ( 'NONE', *, *, #51534, .T. ) ;
#33348=DIRECTION ( 'NONE',  ( 0.8980129913408357867, -0.4399689391117104220, 0.000000000000000000 ) ) ;
#33504=CIRCLE ( 'NONE', #17564, 4.999999999999997335 ) ;
#33512=CARTESIAN_POINT ( 'NONE',  ( 46.00000000000000711, 35.00000000000000000, -46.00000000000000000 ) ) ;
#33523=( GEOMETRIC_REPRESENTATION_CONTEXT ( 3 ) GLOBAL_UNCERTAINTY_ASSIGNED_CONTEXT ( ( #22721 ) ) GLOBAL_UNIT_ASSIGNED_CONTEXT ( ( #29615, #28829, #456 ) ) REPRESENTATION_CONTEXT ( 'NONE', 'WORKASPACE' ) );
#33691=ORIENTED_EDGE ( 'NONE', *, *, #13498, .F. ) ;
#33745=VERTEX_POINT ( 'NONE', #31869 ) ;
#33755=DIRECTION ( 'NONE',  ( 0.9051968626821054187, 0.4249925173346860707, 0.000000000000000000 ) ) ;
#33968=DIRECTION ( 'NONE',  ( 0.000000000000000000, 0.000000000000000000, 1.000000000000000000 ) ) ;
#33969=VERTEX_POINT ( 'NONE', #29159 ) ;
#34004=CARTESIAN_POINT ( 'NONE',  ( 43.33156026654913262, 30.00000000000000355, -51.04247435516399634 ) ) ;
#34094=ORIENTED_EDGE ( 'NONE', *, *, #36588, .T. ) ;
#34188=ORIENTED_EDGE ( 'NONE', *, *, #9303, .F. ) ;
#34298=CARTESIAN_POINT ( 'NONE',  ( 46.00000000000000711, -57.64213562373095101, -46.00000000000000000 ) ) ;
#34299=ADVANCED_BREP_SHAPE_REPRESENTATION ( '', ( #35629, #31742 ), #22569 ) ;
#34353=ADVANCED_FACE ( 'NONE', ( #49282 ), #29296, .F. ) ;
#34501=ORIENTED_EDGE ( 'NONE', *, *, #43355, .T. ) ;
#34566=EDGE_LOOP ( 'NONE', ( #18408, #20070, #39265, #51648 ) ) ;
#34648=ORIENTED_EDGE ( 'NONE', *, *, #17181, .F. ) ;
#34751=VERTEX_POINT ( 'NONE', #45288 ) ;
#34855=ORIENTED_EDGE ( 'NONE', *, *, #23490, .F. ) ;
#34930=CARTESIAN_POINT ( 'NONE',  ( 46.00000000000000711, 35.00000000000000000, -46.00000000000000000 ) ) ;
#34943=LINE ( 'NONE', #26286, #17069 ) ;
#35108=DIRECTION ( 'NONE',  ( 0.000000000000000000, 1.000000000000000000, 0.000000000000000000 ) ) ;
#35357=VERTEX_POINT ( 'NONE', #18391 ) ;
#35403=DIRECTION ( 'NONE',  ( 0.5315839928299667116, 0.000000000000000000, -0.8470055835512242393 ) ) ;
#35563=CIRCLE ( 'NONE', #49847, 4.999999999999997335 ) ;
#35573=LINE ( 'NONE', #21764, #13860 ) ;
#35629=MANIFOLD_SOLID_BREP ( 'Chamfer1', #11139 ) ;
#35683=ORIENTED_EDGE ( 'NONE', *, *, #24403, .T. ) ;
#35689=CIRCLE ( 'NONE', #46594, 9.000000000000001776 ) ;
#35726=APPLICATION_CONTEXT ( 'automotive_design' ) ;
#35810=AXIS2_PLACEMENT_3D ( 'NONE', #33512, #13277, #48516 ) ;
#35864=EDGE_CURVE ( 'NONE', #33745, #16360, #15423, .T. ) ;
#35877=ORIENTED_EDGE ( 'NONE', *, *, #47495, .F. ) ;
#35897=DIRECTION ( 'NONE',  ( 0.000000000000000000, -0.000000000000000000, 1.000000000000000000 ) ) ;
#35931=LINE ( 'NONE', #16482, #4523 ) ;
#35977=ORIENTED_EDGE ( 'NONE', *, *, #32988, .T. ) ;
#36025=DIRECTION ( 'NONE',  ( -0.8838680338115276758, 0.000000000000000000, 0.4677363560876407478 ) ) ;
#36091=CARTESIAN_POINT ( 'NONE',  ( 42.96730897722186171, 30.00000000000000355, -41.16782622478179832 ) ) ;
#36347=CARTESIAN_POINT ( 'NONE',  ( 46.81796867211178181, 28.00000000000000355, -47.30331996785741211 ) ) ;
#36488=SHAPE_DEFINITION_REPRESENTATION ( #30626, #11639 ) ;
#36495=VECTOR ( 'NONE', #5628, 1000.000000000000114 ) ;
#36570=FACE_OUTER_BOUND ( 'NONE', #29679, .T. ) ;
#36588=EDGE_CURVE ( 'NONE', #51365, #51208, #44378, .T. ) ;
#36651=PRODUCT_DEFINITION ( 'UNKNOWN', '', #48565, #7476 ) ;
#36747=CARTESIAN_POINT ( 'NONE',  ( 46.00000000000000711, 35.00000000000000000, -35.00000000000000000 ) ) ;
#36778=ORIENTED_EDGE ( 'NONE', *, *, #20539, .T. ) ;
#36817=STYLED_ITEM ( 'NONE', ( #25174 ), #35629 ) ;
#36842=DIRECTION ( 'NONE',  ( -0.01787127051204794384, -0.8746197071393964073, 0.4844801188631808198 ) ) ;
#37059=EDGE_CURVE ( 'NONE', #30895, #39858, #45714, .T. ) ;
#37070=DIRECTION ( 'NONE',  ( -0.000000000000000000, 1.000000000000000000, -0.000000000000000000 ) ) ;
#37127=AXIS2_PLACEMENT_3D ( 'NONE', #47173, #11148, #27173 ) ;
#37179=DIRECTION ( 'NONE',  ( 0.4106364553079953628, -0.8746197071393964073, 0.2577170336929271999 ) ) ;
#37304=CARTESIAN_POINT ( 'NONE',  ( 46.00000000000000711, -57.64213562373095101, -46.00000000000000000 ) ) ;
#37431=LINE ( 'NONE', #34004, #49106 ) ;
#37510=LINE ( 'NONE', #29616, #1836 ) ;
#37693=ORIENTED_EDGE ( 'NONE', *, *, #9263, .F. ) ;
#37703=CARTESIAN_POINT ( 'NONE',  ( 48.66843973345087448, 30.00000000000000355, -40.95752564483601788 ) ) ;
#37802=VERTEX_POINT ( 'NONE', #46559 ) ;
#37839=DIRECTION ( 'NONE',  ( -0.8470055835512244613, 0.000000000000000000, -0.5315839928299663786 ) ) ;
#37874=EDGE_CURVE ( 'NONE', #27204, #35357, #15268, .T. ) ;
#37901=DIRECTION ( 'NONE',  ( 0.000000000000000000, 0.000000000000000000, 1.000000000000000000 ) ) ;
#37961=ADVANCED_FACE ( 'NONE', ( #48892 ), #28630, .T. ) ;
#38016=PLANE ( 'NONE',  #19286 ) ;
#38053=CARTESIAN_POINT ( 'NONE',  ( 46.00000000000000711, 20.00000000000000000, -35.00000000000000000 ) ) ;
#38272=ORIENTED_EDGE ( 'NONE', *, *, #12642, .T. ) ;
#38322=DIRECTION ( 'NONE',  ( 0.000000000000000000, -1.000000000000000000, 0.000000000000000000 ) ) ;
#38514=ORIENTED_EDGE ( 'NONE', *, *, #24633, .F. ) ;
#38653=CIRCLE ( 'NONE', #7599, 10.99999999999999645 ) ;
#38732=DIRECTION ( 'NONE',  ( 0.000000000000000000, -1.000000000000000000, -0.000000000000000000 ) ) ;
#38744=ADVANCED_FACE ( 'NONE', ( #22771 ), #40343, .T. ) ;
#38777=DIRECTION ( 'NONE',  ( -0.4677363560876381388, 0.000000000000000000, -0.8838680338115288970 ) ) ;
#38780=CARTESIAN_POINT ( 'NONE',  ( 46.00000000000000711, -43.50000000000000000, -46.00000000000000000 ) ) ;
#38884=ORIENTED_EDGE ( 'NONE', *, *, #14054, .F. ) ;
#38968=EDGE_LOOP ( 'NONE', ( #27436, #42091, #27199, #1905 ) ) ;
#39004=ORIENTED_EDGE ( 'NONE', *, *, #13584, .T. ) ;
#39097=AXIS2_PLACEMENT_3D ( 'NONE', #11417, #27454, #3539 ) ;
#39138=CARTESIAN_POINT ( 'NONE',  ( 43.33156026654913262, 35.00000000000000000, -51.04247435516399634 ) ) ;
#39159=DIRECTION ( 'NONE',  ( 0.01787127051204739914, -0.8746197071393964073, -0.4844801188631808198 ) ) ;
#39265=ORIENTED_EDGE ( 'NONE', *, *, #5937, .T. ) ;
#39318=DIRECTION ( 'NONE',  ( 0.000000000000000000, 1.000000000000000000, 0.000000000000000000 ) ) ;
#39323=CARTESIAN_POINT ( 'NONE',  ( 0.000000000000000000, 28.00000000000000355, 0.000000000000000000 ) ) ;
#39552=CARTESIAN_POINT ( 'NONE',  ( 49.03269102277813829, 35.00000000000000000, -50.83217377521822300 ) ) ;
#39637=VERTEX_POINT ( 'NONE', #40930 ) ;
#39646=DIRECTION ( 'NONE',  ( 0.000000000000000000, 1.000000000000000000, 0.000000000000000000 ) ) ;
#39683=PLANE ( 'NONE',  #15774 ) ;
#39738=EDGE_CURVE ( 'NONE', #51208, #22860, #37510, .T. ) ;
#39818=CARTESIAN_POINT ( 'NONE',  ( 51.70113075622899856, 35.00000000000000000, -45.78969942005421956 ) ) ;
#39858=VERTEX_POINT ( 'NONE', #39818 ) ;
#39909=EDGE_CURVE ( 'NONE', #8157, #46358, #4353, .T. ) ;
#40136=CIRCLE ( 'NONE', #14128, 10.99999999999999645 ) ;
#40343=CONICAL_SURFACE ( 'NONE', #47912, 4.000000000000003553, 0.7853981633974479459 ) ;
#40367=VECTOR ( 'NONE', #20416, 1000.000000000000114 ) ;
#40389=SURFACE_SIDE_STYLE ('',( #737 ) ) ;
#40754=VECTOR ( 'NONE', #16078, 1000.000000000000227 ) ;
#40860=ORIENTED_EDGE ( 'NONE', *, *, #45942, .T. ) ;
#40871=VECTOR ( 'NONE', #12106, 1000.000000000000227 ) ;
#40930=CARTESIAN_POINT ( 'NONE',  ( 46.00000000000000711, -43.50000000000000000, -41.99999999999999289 ) ) ;
#41089=CARTESIAN_POINT ( 'NONE',  ( 47.80033453782772312, 28.88712326890129489, -48.86858413038775240 ) ) ;
#41107=VERTEX_POINT ( 'NONE', #30255 ) ;
#41182=LINE ( 'NONE', #1508, #26837 ) ;
#41453=VERTEX_POINT ( 'NONE', #14925 ) ;
#41636=VERTEX_POINT ( 'NONE', #21179 ) ;
#41687=EDGE_CURVE ( 'NONE', #51239, #6148, #32992, .T. ) ;
#41729=AXIS2_PLACEMENT_3D ( 'NONE', #37703, #37179, #33755 ) ;
#41749=PLANE ( 'NONE',  #1593 ) ;
#41800=CARTESIAN_POINT ( 'NONE',  ( 46.00000000000000711, 35.00000000000000000, -55.00000000000000000 ) ) ;
#41810=ORIENTED_EDGE ( 'NONE', *, *, #37059, .T. ) ;
#41849=CARTESIAN_POINT ( 'NONE',  ( 46.00000000000000711, 33.00000000000000000, -46.00000000000000000 ) ) ;
#41968=ADVANCED_FACE ( 'NONE', ( #51136 ), #15121, .T. ) ;
#42091=ORIENTED_EDGE ( 'NONE', *, *, #49994, .F. ) ;
#42111=EDGE_LOOP ( 'NONE', ( #24854, #48398, #49066, #19820 ) ) ;
#42147=DIRECTION ( 'NONE',  ( 0.000000000000000000, 0.000000000000000000, -1.000000000000000000 ) ) ;
#42182=ORIENTED_EDGE ( 'NONE', *, *, #23134, .T. ) ;
#42317=DIRECTION ( 'NONE',  ( 0.8838680338115290080, 0.000000000000000000, -0.4677363560876381943 ) ) ;
#42519=LINE ( 'NONE', #26749, #10588 ) ;
#42584=( NAMED_UNIT ( * ) PLANE_ANGLE_UNIT ( ) SI_UNIT ( $, .RADIAN. ) );
#42990=DIRECTION ( 'NONE',  ( 1.000000000000000000, -0.000000000000000000, 1.224646799147353207E-16 ) ) ;
#43040=DIRECTION ( 'NONE',  ( -0.000000000000000000, -1.000000000000000000, -0.000000000000000000 ) ) ;
#43147=FACE_OUTER_BOUND ( 'NONE', #9841, .T. ) ;
#43227=CIRCLE ( 'NONE', #30612, 4.999999999999997335 ) ;
#43252=FACE_OUTER_BOUND ( 'NONE', #6708, .T. ) ;
#43299=VECTOR ( 'NONE', #21265, 1000.000000000000114 ) ;
#43301=VECTOR ( 'NONE', #15500, 1000.000000000000000 ) ;
#43355=EDGE_CURVE ( 'NONE', #25869, #44162, #15314, .T. ) ;
#43395=AXIS2_PLACEMENT_3D ( 'NONE', #4237, #1528, #3979 ) ;
#43439=CARTESIAN_POINT ( 'NONE',  ( 45.28027613463186185, 28.00000000000000355, -47.36004163347733709 ) ) ;
#43526=CARTESIAN_POINT ( 'NONE',  ( 46.00000000000000711, 20.00000000000000000, -46.00000000000000000 ) ) ;
#43589=EDGE_LOOP ( 'NONE', ( #40860, #920, #25094, #1718 ) ) ;
#43647=ORIENTED_EDGE ( 'NONE', *, *, #4058, .F. ) ;
#43778=ORIENTED_EDGE ( 'NONE', *, *, #51534, .F. ) ;
#43779=ADVANCED_FACE ( 'NONE', ( #31526 ), #16045, .T. ) ;
#43906=ORIENTED_EDGE ( 'NONE', *, *, #17181, .T. ) ;
#43915=ORIENTED_EDGE ( 'NONE', *, *, #24633, .T. ) ;
#43943=AXIS2_PLACEMENT_3D ( 'NONE', #1642, #5063, #49726 ) ;
#43946=CARTESIAN_POINT ( 'NONE',  ( 43.33156026654913262, 30.00000000000000355, -51.04247435516399634 ) ) ;
#44032=ORIENTED_EDGE ( 'NONE', *, *, #39909, .F. ) ;
#44162=VERTEX_POINT ( 'NONE', #47713 ) ;
#44231=ORIENTED_EDGE ( 'NONE', *, *, #46158, .T. ) ;
#44378=LINE ( 'NONE', #11774, #18369 ) ;
#44578=EDGE_CURVE ( 'NONE', #37802, #33969, #25509, .T. ) ;
#44875=ORIENTED_EDGE ( 'NONE', *, *, #1414, .F. ) ;
#45059=AXIS2_PLACEMENT_3D ( 'NONE', #28080, #39646, #8643 ) ;
#45159=CARTESIAN_POINT ( 'NONE',  ( 49.03269102277813829, 35.00000000000000000, -50.83217377521822300 ) ) ;
#45268=DIRECTION ( 'NONE',  ( 0.000000000000000000, -0.4845575045900850641, -0.8747594096352605542 ) ) ;
#45288=CARTESIAN_POINT ( 'NONE',  ( 45.18203132788821108, 28.00000000000000355, -44.69668003214260210 ) ) ;
#45315=DIRECTION ( 'NONE',  ( -0.9993203489176063492, 0.000000000000000000, -0.03686245026030392224 ) ) ;
#45408=DIRECTION ( 'NONE',  ( 0.9993203489176063492, 0.000000000000000000, 0.03686245026030503941 ) ) ;
#45424=AXIS2_PLACEMENT_3D ( 'NONE', #50745, #27062, #2900 ) ;
#45484=ORIENTED_EDGE ( 'NONE', *, *, #12095, .F. ) ;
#45561=CARTESIAN_POINT ( 'NONE',  ( 46.00000000000000711, 33.00000000000000000, -46.00000000000000000 ) ) ;
#45703=AXIS2_PLACEMENT_3D ( 'NONE', #39323, #24329, #11721 ) ;
#45714=LINE ( 'NONE', #21544, #1630 ) ;
#45810=ORIENTED_EDGE ( 'NONE', *, *, #39738, .T. ) ;
#45853=ORIENTED_EDGE ( 'NONE', *, *, #39909, .T. ) ;
#45942=EDGE_CURVE ( 'NONE', #6148, #37802, #34943, .T. ) ;
#46021=EDGE_LOOP ( 'NONE', ( #35683, #15435 ) ) ;
#46102=EDGE_LOOP ( 'NONE', ( #39004, #1256, #16827, #30056 ) ) ;
#46158=EDGE_CURVE ( 'NONE', #27204, #41453, #35563, .T. ) ;
#46358=VERTEX_POINT ( 'NONE', #38053 ) ;
#46390=LINE ( 'NONE', #24919, #12250 ) ;
#46476=CARTESIAN_POINT ( 'NONE',  ( 48.66843973345087448, 30.00000000000000355, -40.95752564483601788 ) ) ;
#46481=EDGE_CURVE ( 'NONE', #33745, #41107, #35931, .T. ) ;
#46535=DIRECTION ( 'NONE',  ( 0.4677363560876406923, 0.000000000000000000, 0.8838680338115276758 ) ) ;
#46559=CARTESIAN_POINT ( 'NONE',  ( 42.96730897722186171, 30.00000000000000355, -41.16782622478179832 ) ) ;
#46594=AXIS2_PLACEMENT_3D ( 'NONE', #22766, #46953, #6994 ) ;
#46692=VERTEX_POINT ( 'NONE', #36347 ) ;
#46738=DIRECTION ( 'NONE',  ( 0.8470055835512242393, 0.000000000000000000, 0.5315839928299667116 ) ) ;
#46739=ORIENTED_EDGE ( 'NONE', *, *, #32988, .F. ) ;
#46953=DIRECTION ( 'NONE',  ( 0.000000000000000000, 1.000000000000000000, 0.000000000000000000 ) ) ;
#46965=CARTESIAN_POINT ( 'NONE',  ( 0.000000000000000000, -43.50000000000000000, 0.000000000000000000 ) ) ;
#47173=CARTESIAN_POINT ( 'NONE',  ( 46.00000000000000711, 35.00000000000000000, -46.00000000000000000 ) ) ;
#47244=VECTOR ( 'NONE', #26678, 1000.000000000000227 ) ;
#47293=ORIENTED_EDGE ( 'NONE', *, *, #47495, .T. ) ;
#47434=PLANE ( 'NONE',  #39097 ) ;
#47495=EDGE_CURVE ( 'NONE', #6148, #2027, #19672, .T. ) ;
#47713=CARTESIAN_POINT ( 'NONE',  ( 43.33156026654913262, 30.00000000000000355, -51.04247435516399634 ) ) ;
#47760=LINE ( 'NONE', #3862, #21668 ) ;
#47802=DIRECTION ( 'NONE',  ( -0.4677363560876381388, 0.000000000000000000, -0.8838680338115288970 ) ) ;
#47820=EDGE_CURVE ( 'NONE', #16360, #46692, #35573, .T. ) ;
#47821=FACE_OUTER_BOUND ( 'NONE', #46102, .T. ) ;
#47865=CARTESIAN_POINT ( 'NONE',  ( 40.29886924377099433, 30.00000000000000355, -46.21030057994576623 ) ) ;
#47912=AXIS2_PLACEMENT_3D ( 'NONE', #38780, #35108, #2786 ) ;
#47988=DIRECTION ( 'NONE',  ( 0.5315839928299667116, 0.000000000000000000, -0.8470055835512242393 ) ) ;
#47999=VECTOR ( 'NONE', #37070, 1000.000000000000000 ) ;
#48341=ORIENTED_EDGE ( 'NONE', *, *, #48592, .F. ) ;
#48398=ORIENTED_EDGE ( 'NONE', *, *, #20491, .T. ) ;
#48457=DIRECTION ( 'NONE',  ( 0.9993203489176063492, 0.000000000000000000, 0.03686245026030503941 ) ) ;
#48516=DIRECTION ( 'NONE',  ( 0.000000000000000000, -0.000000000000000000, 1.000000000000000000 ) ) ;
#48565=PRODUCT_DEFINITION_FORMATION_WITH_SPECIFIED_SOURCE ( 'ANY', '', #13844, .NOT_KNOWN. ) ;
#48592=EDGE_CURVE ( 'NONE', #41107, #30895, #3929, .T. ) ;
#48634=ORIENTED_EDGE ( 'NONE', *, *, #7982, .T. ) ;
#48654=ORIENTED_EDGE ( 'NONE', *, *, #51902, .T. ) ;
#48670=VERTEX_POINT ( 'NONE', #39138 ) ;
#48892=FACE_OUTER_BOUND ( 'NONE', #28597, .T. ) ;
#48904=FACE_OUTER_BOUND ( 'NONE', #19514, .T. ) ;
#49066=ORIENTED_EDGE ( 'NONE', *, *, #37874, .T. ) ;
#49106=VECTOR ( 'NONE', #49279, 1000.000000000000000 ) ;
#49111=EDGE_CURVE ( 'NONE', #46692, #51208, #6142, .T. ) ;
#49162=PLANE ( 'NONE',  #13245 ) ;
#49223=ORIENTED_EDGE ( 'NONE', *, *, #7982, .F. ) ;
#49279=DIRECTION ( 'NONE',  ( -0.000000000000000000, 1.000000000000000000, -0.000000000000000000 ) ) ;
#49282=FACE_OUTER_BOUND ( 'NONE', #38968, .T. ) ;
#49305=CARTESIAN_POINT ( 'NONE',  ( 51.70113075622899856, 30.00000000000000355, -45.78969942005421956 ) ) ;
#49336=ORIENTED_EDGE ( 'NONE', *, *, #20539, .F. ) ;
#49436=DIRECTION ( 'NONE',  ( -0.5315839928299663786, 0.000000000000000000, 0.8470055835512244613 ) ) ;
#49454=CARTESIAN_POINT ( 'NONE',  ( 42.96730897722186171, 30.00000000000000355, -41.16782622478179832 ) ) ;
#49563=AXIS2_PLACEMENT_3D ( 'NONE', #5313, #36842, #45268 ) ;
#49726=DIRECTION ( 'NONE',  ( 0.000000000000000000, 0.000000000000000000, 1.000000000000000000 ) ) ;
#49757=VECTOR ( 'NONE', #14605, 999.9999999999998863 ) ;
#49847=AXIS2_PLACEMENT_3D ( 'NONE', #7614, #20878, #24421 ) ;
#49985=CARTESIAN_POINT ( 'NONE',  ( 46.00000000000000711, -43.50000000000000000, -50.00000000000000000 ) ) ;
#49994=EDGE_CURVE ( 'NONE', #16360, #51365, #5247, .T. ) ;
#50102=CARTESIAN_POINT ( 'NONE',  ( 46.00000000000000711, -43.50000000000000000, -50.00000000000000000 ) ) ;
#50106=EDGE_LOOP ( 'NONE', ( #34094, #51968, #20187, #26917 ) ) ;
#50136=EDGE_CURVE ( 'NONE', #41636, #8157, #42519, .T. ) ;
#50149=VECTOR ( 'NONE', #22880, 999.9999999999998863 ) ;
#50297=VECTOR ( 'NONE', #47988, 1000.000000000000000 ) ;
#50336=ORIENTED_EDGE ( 'NONE', *, *, #44578, .T. ) ;
#50431=FACE_OUTER_BOUND ( 'NONE', #32789, .T. ) ;
#50474=ORIENTED_EDGE ( 'NONE', *, *, #41687, .F. ) ;
#50488=CARTESIAN_POINT ( 'NONE',  ( 51.70113075622899856, 30.00000000000000355, -45.78969942005421956 ) ) ;
#50594=DIRECTION ( 'NONE',  ( -0.5315839928299663786, 0.000000000000000000, 0.8470055835512245723 ) ) ;
#50700=EDGE_CURVE ( 'NONE', #11274, #27379, #8107, .T. ) ;
#50738=SHAPE_REPRESENTATION_RELATIONSHIP ( 'NONE' , 'NONE' ,  #11639, #34299 ) ;
#50745=CARTESIAN_POINT ( 'NONE',  ( 46.00000000000000711, 33.00000000000000000, -46.00000000000000000 ) ) ;
#50914=AXIS2_PLACEMENT_3D ( 'NONE', #34930, #31783, #31249 ) ;
#51098=ORIENTED_EDGE ( 'NONE', *, *, #8991, .T. ) ;
#51136=FACE_OUTER_BOUND ( 'NONE', #14378, .T. ) ;
#51208=VERTEX_POINT ( 'NONE', #19618 ) ;
#51239=VERTEX_POINT ( 'NONE', #18585 ) ;
#51311=CARTESIAN_POINT ( 'NONE',  ( 42.96730897722186171, 30.00000000000000355, -41.16782622478179832 ) ) ;
#51365=VERTEX_POINT ( 'NONE', #49305 ) ;
#51473=CIRCLE ( 'NONE', #24600, 2.000000000000001776 ) ;
#51499=EDGE_LOOP ( 'NONE', ( #19898, #7843, #10725, #43647, #17284, #23524 ) ) ;
#51534=EDGE_CURVE ( 'NONE', #25869, #51239, #2498, .T. ) ;
#51561=LINE ( 'NONE', #15836, #10594 ) ;
#51642=CARTESIAN_POINT ( 'NONE',  ( 46.00000000000000711, 35.00000000000000000, -46.00000000000000000 ) ) ;
#51648=ORIENTED_EDGE ( 'NONE', *, *, #20491, .F. ) ;
#51902=EDGE_CURVE ( 'NONE', #12238, #41636, #40136, .T. ) ;
#51968=ORIENTED_EDGE ( 'NONE', *, *, #49111, .F. ) ;
ENDSEC;
END-ISO-10303-21;
